ISO-10303-21;
HEADER;
FILE_DESCRIPTION (('STEP AP214'),
    '1' );
FILE_NAME ('socket head cap screw_iso_ISO 4762 M5 x 16 - 16N.step',
    '2026-10-08T08:02:49',
    ( '' ),
    ( '' ),
    'SwSTEP 2.0',
    'SolidWorks 2026',
    '' );
FILE_SCHEMA (( 'AUTOMOTIVE_DESIGN' ));
ENDSEC;

DATA;
#50=FILL_AREA_STYLE_COLOUR ( '', #7249 ) ;
#122=CARTESIAN_POINT ( 'NONE',  ( 21.00000000000000355, 2.516649172247811061E-16, -2.055000000000000160 ) ) ;
#271=FACE_OUTER_BOUND ( 'NONE', #58195, .T. ) ;
#282=DIRECTION ( 'NONE',  ( 1.000000000000000000, 0.000000000000000000, 0.000000000000000000 ) ) ;
#320=ADVANCED_FACE ( 'NONE', ( #53535 ), #44196, .F. ) ;
#376=VERTEX_POINT ( 'NONE', #3003 ) ;
#501=ORIENTED_EDGE ( 'NONE', *, *, #49290, .F. ) ;
#633=ORIENTED_EDGE ( 'NONE', *, *, #26342, .T. ) ;
#649=VECTOR ( 'NONE', #57815, 1000.000000000000114 ) ;
#723=DIRECTION ( 'NONE',  ( 1.000000000000000000, 0.000000000000000000, 0.000000000000000000 ) ) ;
#749=CARTESIAN_POINT ( 'NONE',  ( -31.74999999999995737, 0.000000000000000000, 0.000000000000000000 ) ) ;
#770=EDGE_CURVE ( 'NONE', #27059, #18903, #60242, .T. ) ;
#812=( GEOMETRIC_REPRESENTATION_CONTEXT ( 3 ) GLOBAL_UNCERTAINTY_ASSIGNED_CONTEXT ( ( #24190 ) ) GLOBAL_UNIT_ASSIGNED_CONTEXT ( ( #51284, #41927, #36297 ) ) REPRESENTATION_CONTEXT ( 'NONE', 'WORKASPACE' ) );
#878=AXIS2_PLACEMENT_3D ( 'NONE', #55529, #46473, #8857 ) ;
#888=DIRECTION ( 'NONE',  ( -1.000000000000000000, -0.000000000000000000, -0.000000000000000000 ) ) ;
#973=EDGE_CURVE ( 'NONE', #44200, #49037, #20751, .T. ) ;
#1028=DIRECTION ( 'NONE',  ( -1.000000000000000000, -0.000000000000000000, -0.000000000000000000 ) ) ;
#1047=ORIENTED_EDGE ( 'NONE', *, *, #27171, .T. ) ;
#1153=CARTESIAN_POINT ( 'NONE',  ( 0.2500000000000002220, 0.000000000000000000, 0.000000000000000000 ) ) ;
#1265=CARTESIAN_POINT ( 'NONE',  ( 0.000000000000000000, 2.357898499370431722, -2.818925648462311528E-15 ) ) ;
#1527=VERTEX_POINT ( 'NONE', #10151 ) ;
#1571=DIRECTION ( 'NONE',  ( -1.000000000000000000, -0.000000000000000000, -0.000000000000000000 ) ) ;
#1664=AXIS2_PLACEMENT_3D ( 'NONE', #21306, #16611, #35733 ) ;
#1700=FACE_OUTER_BOUND ( 'NONE', #27596, .T. ) ;
#1746=CARTESIAN_POINT ( 'NONE',  ( 0.000000000000000000, 0.000000000000000000, 0.000000000000000000 ) ) ;
#1825=DIRECTION ( 'NONE',  ( -0.000000000000000000, 0.8660254037844392627, 0.4999999999999990008 ) ) ;
#1936=EDGE_LOOP ( 'NONE', ( #501, #5562, #42226, #18781, #54727 ) ) ;
#1952=VECTOR ( 'NONE', #27873, 1000.000000000000000 ) ;
#1963=ADVANCED_FACE ( 'NONE', ( #21874 ), #26877, .T. ) ;
#1992=ORIENTED_EDGE ( 'NONE', *, *, #10301, .F. ) ;
#2015=VERTEX_POINT ( 'NONE', #27486 ) ;
#2171=FACE_OUTER_BOUND ( 'NONE', #44128, .T. ) ;
#2230=PRODUCT_DEFINITION_SHAPE ( 'NONE', 'NONE',  #12658 ) ;
#2376=CARTESIAN_POINT ( 'NONE',  ( 5.200000000000002842, 0.000000000000000000, 0.000000000000000000 ) ) ;
#2593=DIRECTION ( 'NONE',  ( 0.000000000000000000, 0.000000000000000000, 1.000000000000000000 ) ) ;
#2597=EDGE_CURVE ( 'NONE', #18903, #13003, #27644, .T. ) ;
#2671=CIRCLE ( 'NONE', #37728, 2.500000000000000444 ) ;
#2679=EDGE_CURVE ( 'NONE', #32472, #35664, #39232, .T. ) ;
#2738=DIRECTION ( 'NONE',  ( -1.000000000000000000, -0.000000000000000000, -0.000000000000000000 ) ) ;
#2791=DIRECTION ( 'NONE',  ( 0.000000000000000000, 0.4999999999999992784, -0.8660254037844389297 ) ) ;
#2811=ORIENTED_EDGE ( 'NONE', *, *, #52900, .T. ) ;
#3003=CARTESIAN_POINT ( 'NONE',  ( 2.500000000000000000, 1.178949249685212974, -2.042000000000001148 ) ) ;
#3057=FILL_AREA_STYLE ('',( #55057 ) ) ;
#3235=CARTESIAN_POINT ( 'NONE',  ( 4.999999999999997335, 0.000000000000000000, 4.250000000000000000 ) ) ;
#3410=TOROIDAL_SURFACE ( 'NONE', #17429, 4.000000000000000000, 0.2500000000000000000 ) ;
#3448=ADVANCED_FACE ( 'NONE', ( #36463 ), #59899, .F. ) ;
#3577=ORIENTED_EDGE ( 'NONE', *, *, #50850, .T. ) ;
#3616=ORIENTED_EDGE ( 'NONE', *, *, #27171, .F. ) ;
#3705=VERTEX_POINT ( 'NONE', #29190 ) ;
#3759=CARTESIAN_POINT ( 'NONE',  ( 0.000000000000000000, 0.000000000000000000, 0.000000000000000000 ) ) ;
#3816=VECTOR ( 'NONE', #42312, 1000.000000000000114 ) ;
#3839=ORIENTED_EDGE ( 'NONE', *, *, #23280, .F. ) ;
#3882=LINE ( 'NONE', #22701, #41520 ) ;
#3895=EDGE_CURVE ( 'NONE', #49037, #15399, #39906, .T. ) ;
#3932=ORIENTED_EDGE ( 'NONE', *, *, #4714, .F. ) ;
#3937=AXIS2_PLACEMENT_3D ( 'NONE', #59230, #49229, #44260 ) ;
#3989=VERTEX_POINT ( 'NONE', #42323 ) ;
#4097=DIRECTION ( 'NONE',  ( -0.5000000000000051070, 1.060575238724903217E-16, -0.8660254037844355990 ) ) ;
#4213=CARTESIAN_POINT ( 'NONE',  ( 0.2500000000000002220, 0.000000000000000000, 4.250000000000000000 ) ) ;
#4288=ORIENTED_EDGE ( 'NONE', *, *, #4841, .T. ) ;
#4294=EDGE_CURVE ( 'NONE', #22826, #13003, #49381, .T. ) ;
#4335=CARTESIAN_POINT ( 'NONE',  ( 2.500000000000000000, -2.357898499370432166, 3.035766082959412415E-15 ) ) ;
#4714=EDGE_CURVE ( 'NONE', #12101, #3989, #7937, .T. ) ;
#4798=EDGE_CURVE ( 'NONE', #49037, #29670, #17975, .T. ) ;
#4841=EDGE_CURVE ( 'NONE', #2015, #30367, #45981, .T. ) ;
#4901=AXIS2_PLACEMENT_3D ( 'NONE', #38435, #9283, #18701 ) ;
#4948=DIRECTION ( 'NONE',  ( -1.000000000000000000, -0.000000000000000000, -0.000000000000000000 ) ) ;
#5057=VERTEX_POINT ( 'NONE', #24424 ) ;
#5061=AXIS2_PLACEMENT_3D ( 'NONE', #55055, #31895, #12181 ) ;
#5244=DIRECTION ( 'NONE',  ( -1.000000000000000000, -0.000000000000000000, -0.000000000000000000 ) ) ;
#5286=VECTOR ( 'NONE', #6749, 1000.000000000000000 ) ;
#5369=AXIS2_PLACEMENT_3D ( 'NONE', #5958, #15099, #40168 ) ;
#5384=AXIS2_PLACEMENT_3D ( 'NONE', #27538, #17226, #2791 ) ;
#5489=LINE ( 'NONE', #54030, #6444 ) ;
#5562=ORIENTED_EDGE ( 'NONE', *, *, #32687, .F. ) ;
#5598=CARTESIAN_POINT ( 'NONE',  ( 2.500000000000000000, 2.357898499370431722, -2.818925648462311528E-15 ) ) ;
#5688=EDGE_CURVE ( 'NONE', #43133, #3989, #6290, .T. ) ;
#5710=PLANE ( 'NONE',  #57913 ) ;
#5769=AXIS2_PLACEMENT_3D ( 'NONE', #42292, #13164, #32262 ) ;
#5859=AXIS2_PLACEMENT_3D ( 'NONE', #8779, #36697, #61079 ) ;
#5958=CARTESIAN_POINT ( 'NONE',  ( 21.00000000000000355, 0.000000000000000000, 0.000000000000000000 ) ) ;
#6053=ADVANCED_FACE ( 'NONE', ( #49787 ), #52840, .F. ) ;
#6154=LINE ( 'NONE', #43824, #49365 ) ;
#6226=ORIENTED_EDGE ( 'NONE', *, *, #8217, .T. ) ;
#6248=FACE_OUTER_BOUND ( 'NONE', #1936, .T. ) ;
#6290=LINE ( 'NONE', #53917, #14982 ) ;
#6444=VECTOR ( 'NONE', #19948, 1000.000000000000000 ) ;
#6485=VECTOR ( 'NONE', #41593, 1000.000000000000114 ) ;
#6507=ADVANCED_FACE ( 'NONE', ( #21514 ), #46267, .F. ) ;
#6597=ORIENTED_EDGE ( 'NONE', *, *, #47552, .T. ) ;
#6705=AXIS2_PLACEMENT_3D ( 'NONE', #39833, #37873, #29663 ) ;
#6731=AXIS2_PLACEMENT_3D ( 'NONE', #54676, #11805, #30884 ) ;
#6749=DIRECTION ( 'NONE',  ( -1.000000000000000000, -0.000000000000000000, -0.000000000000000000 ) ) ;
#6767=ORIENTED_EDGE ( 'NONE', *, *, #9901, .F. ) ;
#6802=AXIS2_PLACEMENT_3D ( 'NONE', #35948, #32463, #17138 ) ;
#6997=DIRECTION ( 'NONE',  ( -0.5000000000000051070, 0.000000000000000000, 0.8660254037844355990 ) ) ;
#7029=EDGE_CURVE ( 'NONE', #16747, #40146, #12849, .T. ) ;
#7249=COLOUR_RGB ( '', 0.08235294, 0.09019608, 0.10196078) ;
#7387=LINE ( 'NONE', #40650, #44030 ) ;
#7592=CARTESIAN_POINT ( 'NONE',  ( 0.000000000000000000, 5.051668046482832750E-16, -4.000000000000000000 ) ) ;
#7665=CIRCLE ( 'NONE', #42710, 4.250000000000000000 ) ;
#7691=VERTEX_POINT ( 'NONE', #39727 ) ;
#7724=ORIENTED_EDGE ( 'NONE', *, *, #13980, .F. ) ;
#7937=LINE ( 'NONE', #22048, #60080 ) ;
#7948=CARTESIAN_POINT ( 'NONE',  ( 2.500000000000000000, 0.000000000000000000, 2.041999999999999815 ) ) ;
#7991=AXIS2_PLACEMENT_3D ( 'NONE', #15912, #45355, #30601 ) ;
#8018=LINE ( 'NONE', #36548, #39236 ) ;
#8075=SURFACE_STYLE_FILL_AREA ( #3057 ) ;
#8078=DIRECTION ( 'NONE',  ( 0.000000000000000000, 1.224646799147353207E-16, 1.000000000000000000 ) ) ;
#8217=EDGE_CURVE ( 'NONE', #5057, #35220, #35610, .T. ) ;
#8381=DIRECTION ( 'NONE',  ( 0.000000000000000000, 0.000000000000000000, 1.000000000000000000 ) ) ;
#8557=AXIS2_PLACEMENT_3D ( 'NONE', #27994, #52402, #47723 ) ;
#8574=ORIENTED_EDGE ( 'NONE', *, *, #5688, .F. ) ;
#8642=EDGE_LOOP ( 'NONE', ( #23920, #43738 ) ) ;
#8648=PLANE ( 'NONE',  #34532 ) ;
#8725=EDGE_LOOP ( 'NONE', ( #21967, #50733 ) ) ;
#8779=CARTESIAN_POINT ( 'NONE',  ( 0.2500000000000002220, 0.000000000000000000, 0.000000000000000000 ) ) ;
#8800=PRODUCT ( 'socket head cap screw_iso_ISO 4762 M5 x 16 - 16N', 'socket head cap screw_iso_ISO 4762 M5 x 16 - 16N', '', ( #13033 ) ) ;
#8806=DIRECTION ( 'NONE',  ( -1.000000000000000000, -0.000000000000000000, -0.000000000000000000 ) ) ;
#8857=DIRECTION ( 'NONE',  ( 0.000000000000000000, 0.000000000000000000, 1.000000000000000000 ) ) ;
#9062=ORIENTED_EDGE ( 'NONE', *, *, #4798, .T. ) ;
#9072=CARTESIAN_POINT ( 'NONE',  ( 2.500000000000000000, 1.768423874527822459, -1.021000000000002794 ) ) ;
#9089=ORIENTED_EDGE ( 'NONE', *, *, #13073, .F. ) ;
#9125=ORIENTED_EDGE ( 'NONE', *, *, #42028, .F. ) ;
#9156=FILL_AREA_STYLE ('',( #50 ) ) ;
#9225=CARTESIAN_POINT ( 'NONE',  ( 0.2500000000000002220, 5.204748896376250699E-16, -4.250000000000000000 ) ) ;
#9283=DIRECTION ( 'NONE',  ( 1.000000000000000000, 0.000000000000000000, 0.000000000000000000 ) ) ;
#9284=AXIS2_PLACEMENT_3D ( 'NONE', #2376, #59701, #16818 ) ;
#9370=LINE ( 'NONE', #28476, #1952 ) ;
#9405=EDGE_CURVE ( 'NONE', #27059, #50629, #47060, .T. ) ;
#9478=CARTESIAN_POINT ( 'NONE',  ( 0.000000000000000000, -2.357898499370432166, 3.035766082959412415E-15 ) ) ;
#9896=ADVANCED_FACE ( 'NONE', ( #36905 ), #41292, .F. ) ;
#9901=EDGE_CURVE ( 'NONE', #15368, #32472, #50651, .T. ) ;
#9907=EDGE_CURVE ( 'NONE', #18903, #22826, #14541, .T. ) ;
#10060=ORIENTED_EDGE ( 'NONE', *, *, #49290, .T. ) ;
#10151=CARTESIAN_POINT ( 'NONE',  ( 0.000000000000000000, -1.178949249685214307, 2.042000000000001592 ) ) ;
#10301=EDGE_CURVE ( 'NONE', #13003, #3705, #46454, .T. ) ;
#10346=EDGE_LOOP ( 'NONE', ( #17085, #9062, #22073, #17670 ) ) ;
#10530=DIRECTION ( 'NONE',  ( 0.000000000000000000, 0.000000000000000000, 1.000000000000000000 ) ) ;
#10855=CARTESIAN_POINT ( 'NONE',  ( 2.500000000000000000, -2.357898499370432166, 3.035766082959412415E-15 ) ) ;
#11067=ORIENTED_EDGE ( 'NONE', *, *, #46212, .F. ) ;
#11320=VECTOR ( 'NONE', #18037, 1000.000000000000114 ) ;
#11347=DIRECTION ( 'NONE',  ( -1.000000000000000000, -0.000000000000000000, -0.000000000000000000 ) ) ;
#11453=DIRECTION ( 'NONE',  ( -1.000000000000000000, -0.000000000000000000, -0.000000000000000000 ) ) ;
#11691=AXIS2_PLACEMENT_3D ( 'NONE', #749, #25176, #19885 ) ;
#11713=CARTESIAN_POINT ( 'NONE',  ( -31.74999999999995737, 0.000000000000000000, 0.000000000000000000 ) ) ;
#11755=DIRECTION ( 'NONE',  ( -1.000000000000000000, -0.000000000000000000, -0.000000000000000000 ) ) ;
#11759=FACE_OUTER_BOUND ( 'NONE', #54226, .T. ) ;
#11805=DIRECTION ( 'NONE',  ( -1.000000000000000000, -0.000000000000000000, -0.000000000000000000 ) ) ;
#11847=MECHANICAL_DESIGN_GEOMETRIC_PRESENTATION_REPRESENTATION('',(#34860),#812);
#11870=AXIS2_PLACEMENT_3D ( 'NONE', #25671, #49167, #40121 ) ;
#11893=COLOUR_RGB ( '', 0.08235294, 0.09019608, 0.10196078) ;
#11932=AXIS2_PLACEMENT_3D ( 'NONE', #22478, #55979, #46611 ) ;
#11934=PLANE ( 'NONE',  #1664 ) ;
#12083=DIRECTION ( 'NONE',  ( 0.000000000000000000, 0.5000000000000011102, 0.8660254037844379305 ) ) ;
#12101=VERTEX_POINT ( 'NONE', #46244 ) ;
#12181=DIRECTION ( 'NONE',  ( 0.000000000000000000, 0.000000000000000000, -1.000000000000000000 ) ) ;
#12189=EDGE_CURVE ( 'NONE', #35220, #57870, #35815, .T. ) ;
#12390=AXIS2_PLACEMENT_3D ( 'NONE', #16459, #20548, #10530 ) ;
#12506=ORIENTED_EDGE ( 'NONE', *, *, #26342, .F. ) ;
#12607=EDGE_LOOP ( 'NONE', ( #58524, #4288, #44446, #61322 ) ) ;
#12613=ORIENTED_EDGE ( 'NONE', *, *, #24008, .T. ) ;
#12658=PRODUCT_DEFINITION ( 'UNKNOWN', '', #58888, #56162 ) ;
#12849=CIRCLE ( 'NONE', #20827, 2.055000000000000160 ) ;
#13003=VERTEX_POINT ( 'NONE', #41711 ) ;
#13008=ORIENTED_EDGE ( 'NONE', *, *, #9405, .T. ) ;
#13033=PRODUCT_CONTEXT ( 'NONE', #51153, 'mechanical' ) ;
#13073=EDGE_CURVE ( 'NONE', #5057, #35775, #2671, .T. ) ;
#13164=DIRECTION ( 'NONE',  ( -1.000000000000000000, -0.000000000000000000, -0.000000000000000000 ) ) ;
#13360=ORIENTED_EDGE ( 'NONE', *, *, #5688, .T. ) ;
#13392=CARTESIAN_POINT ( 'NONE',  ( 2.500000000000000000, 0.000000000000000000, 0.000000000000000000 ) ) ;
#13400=LINE ( 'NONE', #18405, #31811 ) ;
#13771=ORIENTED_EDGE ( 'NONE', *, *, #52900, .F. ) ;
#13822=DIRECTION ( 'NONE',  ( 1.000000000000000000, 0.000000000000000000, 0.000000000000000000 ) ) ;
#13853=EDGE_LOOP ( 'NONE', ( #35225, #59638, #10060, #58161, #3932, #57013 ) ) ;
#13902=CARTESIAN_POINT ( 'NONE',  ( 2.500000000000000000, 1.768423874527823791, 1.020999999999998353 ) ) ;
#13977=CARTESIAN_POINT ( 'NONE',  ( 0.000000000000000000, -2.357898499370432166, 3.035766082959412415E-15 ) ) ;
#13980=EDGE_CURVE ( 'NONE', #35775, #57870, #46664, .T. ) ;
#14178=ADVANCED_FACE ( 'NONE', ( #58358 ), #43702, .T. ) ;
#14192=CARTESIAN_POINT ( 'NONE',  ( -31.74999999999995737, 3.061616997868383634E-16, -2.500000000000000444 ) ) ;
#14218=CARTESIAN_POINT ( 'NONE',  ( 0.2500000000000002220, 0.000000000000000000, 0.000000000000000000 ) ) ;
#14314=ADVANCED_FACE ( 'NONE', ( #36452 ), #50218, .T. ) ;
#14316=PLANE ( 'NONE',  #4901 ) ;
#14487=CARTESIAN_POINT ( 'NONE',  ( 2.500000000000000000, -2.357898499370432166, 3.035766082959412415E-15 ) ) ;
#14541=CIRCLE ( 'NONE', #21497, 2.041999999999999815 ) ;
#14624=CARTESIAN_POINT ( 'NONE',  ( 2.500000000000000000, -1.178949249685218748, -2.041999999999998039 ) ) ;
#14677=AXIS2_PLACEMENT_3D ( 'NONE', #3759, #61387, #13822 ) ;
#14763=AXIS2_PLACEMENT_3D ( 'NONE', #50033, #26841, #35646 ) ;
#14982=VECTOR ( 'NONE', #31068, 1000.000000000000000 ) ;
#15099=DIRECTION ( 'NONE',  ( -1.000000000000000000, -0.000000000000000000, -0.000000000000000000 ) ) ;
#15191=DIRECTION ( 'NONE',  ( -0.000000000000000000, 1.287488025362403787E-15, 1.000000000000000000 ) ) ;
#15237=FACE_OUTER_BOUND ( 'NONE', #39793, .T. ) ;
#15262=DIRECTION ( 'NONE',  ( 0.000000000000000000, 0.000000000000000000, 1.000000000000000000 ) ) ;
#15359=DIRECTION ( 'NONE',  ( 1.000000000000000000, 0.000000000000000000, 0.000000000000000000 ) ) ;
#15368=VERTEX_POINT ( 'NONE', #41866 ) ;
#15399=VERTEX_POINT ( 'NONE', #4213 ) ;
#15417=ORIENTED_EDGE ( 'NONE', *, *, #45373, .F. ) ;
#15552=EDGE_LOOP ( 'NONE', ( #54777, #56630 ) ) ;
#15912=CARTESIAN_POINT ( 'NONE',  ( 2.500000000000000000, 0.000000000000000000, 0.000000000000000000 ) ) ;
#16225=LINE ( 'NONE', #54099, #18793 ) ;
#16348=EDGE_CURVE ( 'NONE', #16747, #30367, #8018, .T. ) ;
#16437=CARTESIAN_POINT ( 'NONE',  ( 4.999999999999997335, 0.000000000000000000, 0.000000000000000000 ) ) ;
#16459=CARTESIAN_POINT ( 'NONE',  ( 0.000000000000000000, 0.000000000000000000, 0.000000000000000000 ) ) ;
#16604=ORIENTED_EDGE ( 'NONE', *, *, #53172, .F. ) ;
#16611=DIRECTION ( 'NONE',  ( 1.000000000000000000, 0.000000000000000000, 0.000000000000000000 ) ) ;
#16683=ORIENTED_EDGE ( 'NONE', *, *, #44099, .T. ) ;
#16747=VERTEX_POINT ( 'NONE', #32709 ) ;
#16818=DIRECTION ( 'NONE',  ( 0.000000000000000000, 0.000000000000000000, -1.000000000000000000 ) ) ;
#16834=ORIENTED_EDGE ( 'NONE', *, *, #16857, .T. ) ;
#16857=EDGE_CURVE ( 'NONE', #48312, #12101, #43351, .T. ) ;
#16862=CARTESIAN_POINT ( 'NONE',  ( 2.500000000000000000, 2.357898499370431722, -2.818925648462311528E-15 ) ) ;
#17085=ORIENTED_EDGE ( 'NONE', *, *, #3895, .F. ) ;
#17112=PLANE ( 'NONE',  #60050 ) ;
#17138=DIRECTION ( 'NONE',  ( 0.000000000000000000, 0.000000000000000000, -1.000000000000000000 ) ) ;
#17226=DIRECTION ( 'NONE',  ( 0.000000000000000000, -0.8660254037844390407, -0.4999999999999993339 ) ) ;
#17324=DIRECTION ( 'NONE',  ( -1.000000000000000000, -0.000000000000000000, -0.000000000000000000 ) ) ;
#17429=AXIS2_PLACEMENT_3D ( 'NONE', #46166, #55525, #21720 ) ;
#17450=CARTESIAN_POINT ( 'NONE',  ( 2.500000000000000000, 2.357898499370431722, -2.818925648462311528E-15 ) ) ;
#17457=EDGE_CURVE ( 'NONE', #7691, #29670, #43303, .T. ) ;
#17495=CIRCLE ( 'NONE', #45499, 2.041999999999999815 ) ;
#17549=EDGE_CURVE ( 'NONE', #57870, #35220, #21281, .T. ) ;
#17631=AXIS2_PLACEMENT_3D ( 'NONE', #56608, #21881, #8078 ) ;
#17670=ORIENTED_EDGE ( 'NONE', *, *, #29056, .F. ) ;
#17803=CARTESIAN_POINT ( 'NONE',  ( 20.55500000000001748, 0.000000000000000000, 2.500000000000000888 ) ) ;
#17975=CIRCLE ( 'NONE', #39004, 0.2500000000000002220 ) ;
#18035=CARTESIAN_POINT ( 'NONE',  ( 2.500000000000000000, -1.178949249685214307, 2.042000000000001592 ) ) ;
#18037=DIRECTION ( 'NONE',  ( -0.7071067811865364705, 8.659560562355067211E-17, -0.7071067811865584529 ) ) ;
#18405=CARTESIAN_POINT ( 'NONE',  ( 2.500000000000000000, 1.178949249685212974, -2.042000000000001148 ) ) ;
#18449=CARTESIAN_POINT ( 'NONE',  ( 4.999999999999997335, 0.000000000000000000, 0.000000000000000000 ) ) ;
#18607=DIRECTION ( 'NONE',  ( 0.000000000000000000, -0.5000000000000013323, -0.8660254037844380415 ) ) ;
#18701=DIRECTION ( 'NONE',  ( 0.000000000000000000, 0.000000000000000000, -1.000000000000000000 ) ) ;
#18781=ORIENTED_EDGE ( 'NONE', *, *, #9901, .T. ) ;
#18793=VECTOR ( 'NONE', #50047, 1000.000000000000000 ) ;
#18892=DIRECTION ( 'NONE',  ( -1.000000000000000000, -0.000000000000000000, -0.000000000000000000 ) ) ;
#18893=ORIENTED_EDGE ( 'NONE', *, *, #39281, .F. ) ;
#18903=VERTEX_POINT ( 'NONE', #30859 ) ;
#18918=DIRECTION ( 'NONE',  ( 1.000000000000000000, 0.000000000000000000, 0.000000000000000000 ) ) ;
#19075=ORIENTED_EDGE ( 'NONE', *, *, #48978, .F. ) ;
#19097=ORIENTED_EDGE ( 'NONE', *, *, #16348, .F. ) ;
#19198=SURFACE_SIDE_STYLE ('',( #27962 ) ) ;
#19508=AXIS2_PLACEMENT_3D ( 'NONE', #36813, #22077, #12083 ) ;
#19550=DIRECTION ( 'NONE',  ( 0.000000000000000000, 0.000000000000000000, 1.000000000000000000 ) ) ;
#19591=ORIENTED_EDGE ( 'NONE', *, *, #37617, .T. ) ;
#19592=ORIENTED_EDGE ( 'NONE', *, *, #4294, .T. ) ;
#19616=CARTESIAN_POINT ( 'NONE',  ( 5.200000000000002842, 0.000000000000000000, 0.000000000000000000 ) ) ;
#19619=SHAPE_REPRESENTATION ( 'socket head cap screw_iso_ISO 4762 M5 x 16 - 16N', ( #14677 ), #38903 ) ;
#19706=LINE ( 'NONE', #29093, #52935 ) ;
#19709=EDGE_LOOP ( 'NONE', ( #32074, #55233, #50193, #41287, #31629 ) ) ;
#19831=VERTEX_POINT ( 'NONE', #9072 ) ;
#19859=FACE_OUTER_BOUND ( 'NONE', #24275, .T. ) ;
#19885=DIRECTION ( 'NONE',  ( 0.000000000000000000, 0.000000000000000000, 1.000000000000000000 ) ) ;
#19901=FACE_OUTER_BOUND ( 'NONE', #27081, .T. ) ;
#19948=DIRECTION ( 'NONE',  ( -1.000000000000000000, -0.000000000000000000, -0.000000000000000000 ) ) ;
#20182=CARTESIAN_POINT ( 'NONE',  ( 2.500000000000000000, 2.357898499370431722, -2.818925648462311528E-15 ) ) ;
#20184=ADVANCED_FACE ( 'NONE', ( #58438 ), #53684, .F. ) ;
#20284=LINE ( 'NONE', #44716, #5286 ) ;
#20289=DIRECTION ( 'NONE',  ( -1.000000000000000000, -0.000000000000000000, -0.000000000000000000 ) ) ;
#20328=ORIENTED_EDGE ( 'NONE', *, *, #20397, .F. ) ;
#20354=DIRECTION ( 'NONE',  ( 0.000000000000000000, 0.000000000000000000, -1.000000000000000000 ) ) ;
#20397=EDGE_CURVE ( 'NONE', #27345, #15368, #51210, .T. ) ;
#20548=DIRECTION ( 'NONE',  ( -1.000000000000000000, -0.000000000000000000, -0.000000000000000000 ) ) ;
#20602=DIRECTION ( 'NONE',  ( 0.000000000000000000, -1.000000000000000000, 1.287488025362403787E-15 ) ) ;
#20694=FACE_OUTER_BOUND ( 'NONE', #27835, .T. ) ;
#20706=DIRECTION ( 'NONE',  ( 0.000000000000000000, 0.000000000000000000, 1.000000000000000000 ) ) ;
#20751=LINE ( 'NONE', #54227, #44126 ) ;
#20827=AXIS2_PLACEMENT_3D ( 'NONE', #23122, #36935, #8381 ) ;
#20878=VECTOR ( 'NONE', #35571, 1000.000000000000000 ) ;
#20953=DIRECTION ( 'NONE',  ( 0.000000000000000000, -0.4999999999999989453, 0.8660254037844391517 ) ) ;
#21015=CIRCLE ( 'NONE', #45045, 2.041999999999999815 ) ;
#21103=FACE_OUTER_BOUND ( 'NONE', #36859, .T. ) ;
#21170=DIRECTION ( 'NONE',  ( -1.000000000000000000, -0.000000000000000000, -0.000000000000000000 ) ) ;
#21281=CIRCLE ( 'NONE', #56275, 2.700000000000000622 ) ;
#21306=CARTESIAN_POINT ( 'NONE',  ( 2.500000000000000000, 2.357898499370431722, -2.818925648462311528E-15 ) ) ;
#21489=VERTEX_POINT ( 'NONE', #13977 ) ;
#21497=AXIS2_PLACEMENT_3D ( 'NONE', #60348, #36581, #55040 ) ;
#21514=FACE_OUTER_BOUND ( 'NONE', #58566, .T. ) ;
#21680=TOROIDAL_SURFACE ( 'NONE', #27722, 4.000000000000000000, 0.2500000000000000000 ) ;
#21720=DIRECTION ( 'NONE',  ( 0.000000000000000000, 0.000000000000000000, 1.000000000000000000 ) ) ;
#21855=EDGE_LOOP ( 'NONE', ( #9125, #18893 ) ) ;
#21866=ORIENTED_EDGE ( 'NONE', *, *, #7029, .T. ) ;
#21874=FACE_OUTER_BOUND ( 'NONE', #8642, .T. ) ;
#21881=DIRECTION ( 'NONE',  ( 0.000000000000000000, 1.000000000000000000, -1.224646799147353207E-16 ) ) ;
#21967=ORIENTED_EDGE ( 'NONE', *, *, #12189, .T. ) ;
#22048=CARTESIAN_POINT ( 'NONE',  ( 0.000000000000000000, 1.178949249685212974, -2.042000000000001148 ) ) ;
#22073=ORIENTED_EDGE ( 'NONE', *, *, #17457, .F. ) ;
#22077=DIRECTION ( 'NONE',  ( 0.000000000000000000, 0.8660254037844380415, -0.5000000000000012212 ) ) ;
#22129=VECTOR ( 'NONE', #24799, 1000.000000000000114 ) ;
#22385=EDGE_LOOP ( 'NONE', ( #60194, #44417, #38280, #53803 ) ) ;
#22469=VECTOR ( 'NONE', #37460, 1000.000000000000114 ) ;
#22478=CARTESIAN_POINT ( 'NONE',  ( 0.2500000000000002220, 0.000000000000000000, 4.000000000000000000 ) ) ;
#22487=SHAPE_REPRESENTATION_RELATIONSHIP ( 'NONE' , 'NONE' ,  #19619, #35493 ) ;
#22550=ORIENTED_EDGE ( 'NONE', *, *, #50068, .T. ) ;
#22701=CARTESIAN_POINT ( 'NONE',  ( 0.000000000000000000, 2.357898499370431722, -2.818925648462311528E-15 ) ) ;
#22763=DIRECTION ( 'NONE',  ( 1.000000000000000000, 0.000000000000000000, 0.000000000000000000 ) ) ;
#22781=EDGE_CURVE ( 'NONE', #21489, #3989, #47101, .T. ) ;
#22795=( LENGTH_UNIT ( ) NAMED_UNIT ( * ) SI_UNIT ( .MILLI., .METRE. ) );
#22826=VERTEX_POINT ( 'NONE', #13902 ) ;
#22832=ORIENTED_EDGE ( 'NONE', *, *, #16348, .T. ) ;
#23111=( NAMED_UNIT ( * ) SI_UNIT ( $, .STERADIAN. ) SOLID_ANGLE_UNIT ( ) );
#23122=CARTESIAN_POINT ( 'NONE',  ( 21.00000000000000355, 0.000000000000000000, 0.000000000000000000 ) ) ;
#23168=CARTESIAN_POINT ( 'NONE',  ( 2.500000000000000000, 2.357898499370431722, -2.818925648462311528E-15 ) ) ;
#23179=VERTEX_POINT ( 'NONE', #23168 ) ;
#23183=CARTESIAN_POINT ( 'NONE',  ( 0.000000000000000000, -1.178949249685214307, 2.042000000000001592 ) ) ;
#23258=CARTESIAN_POINT ( 'NONE',  ( 2.500000000000000000, -1.178949249685214307, 2.042000000000001592 ) ) ;
#23280=EDGE_CURVE ( 'NONE', #32472, #21489, #19706, .T. ) ;
#23741=AXIS2_PLACEMENT_3D ( 'NONE', #19616, #25220, #38736 ) ;
#23920=ORIENTED_EDGE ( 'NONE', *, *, #7029, .F. ) ;
#24008=EDGE_CURVE ( 'NONE', #27345, #18903, #9370, .T. ) ;
#24077=DIRECTION ( 'NONE',  ( 0.000000000000000000, 0.000000000000000000, 1.000000000000000000 ) ) ;
#24105=LINE ( 'NONE', #23183, #3816 ) ;
#24189=DIRECTION ( 'NONE',  ( -0.000000000000000000, 1.000000000000000000, 1.224646799147353207E-16 ) ) ;
#24190=UNCERTAINTY_MEASURE_WITH_UNIT (LENGTH_MEASURE( 1.000000000000000082E-05 ), #51284, 'distance_accuracy_value', 'NONE');
#24272=( GEOMETRIC_REPRESENTATION_CONTEXT ( 3 ) GLOBAL_UNCERTAINTY_ASSIGNED_CONTEXT ( ( #59938 ) ) GLOBAL_UNIT_ASSIGNED_CONTEXT ( ( #42091, #51753, #38613 ) ) REPRESENTATION_CONTEXT ( 'NONE', 'WORKASPACE' ) );
#24275=EDGE_LOOP ( 'NONE', ( #21866, #22550, #31297, #19097 ) ) ;
#24313=CIRCLE ( 'NONE', #9284, 2.500000000000000444 ) ;
#24424=CARTESIAN_POINT ( 'NONE',  ( 5.200000000000002842, 3.061616997868383634E-16, -2.500000000000000444 ) ) ;
#24474=CARTESIAN_POINT ( 'NONE',  ( 3.678949249685231848, 0.000000000000000000, 0.000000000000000000 ) ) ;
#24545=FACE_BOUND ( 'NONE', #8725, .T. ) ;
#24650=DIRECTION ( 'NONE',  ( -1.000000000000000000, -0.000000000000000000, -0.000000000000000000 ) ) ;
#24799=DIRECTION ( 'NONE',  ( 0.000000000000000000, 0.4999999999999990008, -0.8660254037844391517 ) ) ;
#24918=ORIENTED_EDGE ( 'NONE', *, *, #31598, .T. ) ;
#25176=DIRECTION ( 'NONE',  ( -1.000000000000000000, -0.000000000000000000, -0.000000000000000000 ) ) ;
#25220=DIRECTION ( 'NONE',  ( 1.000000000000000000, 0.000000000000000000, 0.000000000000000000 ) ) ;
#25390=CARTESIAN_POINT ( 'NONE',  ( 2.500000000000000000, -1.178949249685214307, 2.042000000000001592 ) ) ;
#25392=ADVANCED_FACE ( 'NONE', ( #35297, #60002 ), #17112, .T. ) ;
#25671=CARTESIAN_POINT ( 'NONE',  ( 5.200000000000002842, 0.000000000000000000, 0.000000000000000000 ) ) ;
#25677=AXIS2_PLACEMENT_3D ( 'NONE', #43790, #24650, #15262 ) ;
#25703=PLANE ( 'NONE',  #58678 ) ;
#26214=DIRECTION ( 'NONE',  ( 0.000000000000000000, -0.5000000000000013323, -0.8660254037844380415 ) ) ;
#26232=DIRECTION ( 'NONE',  ( 1.000000000000000000, 0.000000000000000000, 0.000000000000000000 ) ) ;
#26245=CARTESIAN_POINT ( 'NONE',  ( 2.500000000000000000, -1.178949249685214307, 2.042000000000001592 ) ) ;
#26299=ADVANCED_FACE ( 'NONE', ( #15237 ), #14316, .F. ) ;
#26342=EDGE_CURVE ( 'NONE', #376, #12101, #45296, .T. ) ;
#26370=ORIENTED_EDGE ( 'NONE', *, *, #2679, .F. ) ;
#26450=CARTESIAN_POINT ( 'NONE',  ( 2.500000000000000000, 1.178949249685212974, -2.042000000000001148 ) ) ;
#26499=DIRECTION ( 'NONE',  ( 0.000000000000000000, -0.4999999999999993339, 0.8660254037844390407 ) ) ;
#26596=ORIENTED_EDGE ( 'NONE', *, *, #8217, .F. ) ;
#26798=SHAPE_DEFINITION_REPRESENTATION ( #2230, #19619 ) ;
#26841=DIRECTION ( 'NONE',  ( -1.000000000000000000, -0.000000000000000000, -0.000000000000000000 ) ) ;
#26877=PLANE ( 'NONE',  #5061 ) ;
#26915=ORIENTED_EDGE ( 'NONE', *, *, #9907, .F. ) ;
#27027=DIRECTION ( 'NONE',  ( 0.000000000000000000, 0.000000000000000000, 1.000000000000000000 ) ) ;
#27059=VERTEX_POINT ( 'NONE', #24474 ) ;
#27076=PLANE ( 'NONE',  #30882 ) ;
#27081=EDGE_LOOP ( 'NONE', ( #30444, #1992, #50124, #41727, #39108 ) ) ;
#27139=ORIENTED_EDGE ( 'NONE', *, *, #22781, .F. ) ;
#27171=EDGE_CURVE ( 'NONE', #50629, #43133, #13400, .T. ) ;
#27221=CARTESIAN_POINT ( 'NONE',  ( 2.500000000000000000, -2.629050547790028551E-15, -2.041999999999999815 ) ) ;
#27345=VERTEX_POINT ( 'NONE', #54967 ) ;
#27486=CARTESIAN_POINT ( 'NONE',  ( 20.55500000000001748, 3.061616997868384127E-16, -2.500000000000000888 ) ) ;
#27538=CARTESIAN_POINT ( 'NONE',  ( 2.500000000000000000, 2.357898499370431722, -2.818925648462311528E-15 ) ) ;
#27596=EDGE_LOOP ( 'NONE', ( #52237, #54780, #35645, #26596 ) ) ;
#27644=LINE ( 'NONE', #23258, #47144 ) ;
#27722=AXIS2_PLACEMENT_3D ( 'NONE', #1153, #20289, #39407 ) ;
#27732=EDGE_CURVE ( 'NONE', #19831, #376, #49585, .T. ) ;
#27755=AXIS2_PLACEMENT_3D ( 'NONE', #16437, #11755, #34947 ) ;
#27835=EDGE_LOOP ( 'NONE', ( #28013, #31377, #22832, #56307 ) ) ;
#27854=ADVANCED_FACE ( 'NONE', ( #56133 ), #46772, .T. ) ;
#27869=CARTESIAN_POINT ( 'NONE',  ( 4.999999999999997335, 5.204748896376250699E-16, -4.250000000000000000 ) ) ;
#27873=DIRECTION ( 'NONE',  ( 0.000000000000000000, 1.000000000000000000, -1.287488025362403787E-15 ) ) ;
#27962=SURFACE_STYLE_FILL_AREA ( #9156 ) ;
#27994=CARTESIAN_POINT ( 'NONE',  ( 5.200000000000002842, 0.000000000000000000, -2.700000000000000622 ) ) ;
#28013=ORIENTED_EDGE ( 'NONE', *, *, #50068, .F. ) ;
#28207=ORIENTED_EDGE ( 'NONE', *, *, #34542, .T. ) ;
#28355=ORIENTED_EDGE ( 'NONE', *, *, #36461, .T. ) ;
#28447=DIRECTION ( 'NONE',  ( 0.000000000000000000, 0.000000000000000000, 1.000000000000000000 ) ) ;
#28476=CARTESIAN_POINT ( 'NONE',  ( 2.500000000000000000, -1.178949249685214307, 2.042000000000001592 ) ) ;
#28533=CARTESIAN_POINT ( 'NONE',  ( 2.500000000000000000, 2.500728763858895382E-16, -2.041999999999999815 ) ) ;
#28744=CIRCLE ( 'NONE', #39783, 4.250000000000000000 ) ;
#28815=ORIENTED_EDGE ( 'NONE', *, *, #41326, .F. ) ;
#29012=CIRCLE ( 'NONE', #7991, 2.041999999999999815 ) ;
#29056=EDGE_CURVE ( 'NONE', #15399, #7691, #50883, .T. ) ;
#29093=CARTESIAN_POINT ( 'NONE',  ( 2.500000000000000000, -2.357898499370432166, 3.035766082959412415E-15 ) ) ;
#29190=CARTESIAN_POINT ( 'NONE',  ( 0.000000000000000000, 1.178949249685217415, 2.041999999999998483 ) ) ;
#29195=DIRECTION ( 'NONE',  ( 0.000000000000000000, -1.224646799147353454E-16, 1.000000000000000000 ) ) ;
#29663=DIRECTION ( 'NONE',  ( 0.000000000000000000, 0.000000000000000000, 1.000000000000000000 ) ) ;
#29670=VERTEX_POINT ( 'NONE', #7592 ) ;
#29886=CARTESIAN_POINT ( 'NONE',  ( 5.000000000000002665, 3.306546357697854226E-16, 2.700000000000000622 ) ) ;
#30040=CLOSED_SHELL ( 'NONE', ( #3448, #40982, #42458, #52372, #42202, #27854, #25392, #14314, #43647, #14178, #47204, #1963, #6053, #34453, #51751, #57869, #40901, #49355, #42531, #55015, #320, #6507, #61576, #9896, #54721, #26299, #20184 ) ) ;
#30307=DIRECTION ( 'NONE',  ( -1.000000000000000000, -0.000000000000000000, -0.000000000000000000 ) ) ;
#30326=LINE ( 'NONE', #26245, #44381 ) ;
#30367=VERTEX_POINT ( 'NONE', #17803 ) ;
#30444=ORIENTED_EDGE ( 'NONE', *, *, #42528, .T. ) ;
#30539=CARTESIAN_POINT ( 'NONE',  ( 2.500000000000000000, 1.178949249685212974, -2.042000000000001148 ) ) ;
#30601=DIRECTION ( 'NONE',  ( 0.000000000000000000, 0.000000000000000000, 1.000000000000000000 ) ) ;
#30641=PLANE ( 'NONE',  #38876 ) ;
#30720=MANIFOLD_SOLID_BREP ( 'Hex', #30040 ) ;
#30859=CARTESIAN_POINT ( 'NONE',  ( 2.500000000000000000, 2.629050547790028946E-15, 2.042000000000000259 ) ) ;
#30869=CARTESIAN_POINT ( 'NONE',  ( 2.500000000000000000, 0.000000000000000000, 0.000000000000000000 ) ) ;
#30882=AXIS2_PLACEMENT_3D ( 'NONE', #26450, #36493, #60260 ) ;
#30884=DIRECTION ( 'NONE',  ( 0.000000000000000000, 0.000000000000000000, -1.000000000000000000 ) ) ;
#31068=DIRECTION ( 'NONE',  ( -1.000000000000000000, -0.000000000000000000, -0.000000000000000000 ) ) ;
#31269=SURFACE_SIDE_STYLE ('',( #8075 ) ) ;
#31297=ORIENTED_EDGE ( 'NONE', *, *, #47552, .F. ) ;
#31377=ORIENTED_EDGE ( 'NONE', *, *, #33681, .T. ) ;
#31469=FACE_OUTER_BOUND ( 'NONE', #52335, .T. ) ;
#31598=EDGE_CURVE ( 'NONE', #23179, #48312, #20284, .T. ) ;
#31604=EDGE_CURVE ( 'NONE', #35775, #5057, #24313, .T. ) ;
#31629=ORIENTED_EDGE ( 'NONE', *, *, #46094, .T. ) ;
#31645=CARTESIAN_POINT ( 'NONE',  ( 2.500000000000000000, 0.000000000000000000, 0.000000000000000000 ) ) ;
#31811=VECTOR ( 'NONE', #32502, 1000.000000000000000 ) ;
#31852=AXIS2_PLACEMENT_3D ( 'NONE', #60212, #17324, #27027 ) ;
#31895=DIRECTION ( 'NONE',  ( 1.000000000000000000, 0.000000000000000000, 0.000000000000000000 ) ) ;
#32057=EDGE_CURVE ( 'NONE', #29670, #7691, #37390, .T. ) ;
#32074=ORIENTED_EDGE ( 'NONE', *, *, #9405, .F. ) ;
#32204=PRESENTATION_STYLE_ASSIGNMENT (( #45695 ) ) ;
#32262=DIRECTION ( 'NONE',  ( 0.000000000000000000, 0.000000000000000000, 1.000000000000000000 ) ) ;
#32286=MECHANICAL_DESIGN_GEOMETRIC_PRESENTATION_REPRESENTATION('',(#54242),#24272);
#32463=DIRECTION ( 'NONE',  ( 1.000000000000000000, 0.000000000000000000, 0.000000000000000000 ) ) ;
#32472=VERTEX_POINT ( 'NONE', #4335 ) ;
#32502=DIRECTION ( 'NONE',  ( 0.000000000000000000, -1.000000000000000000, 1.287488025362403787E-15 ) ) ;
#32627=CARTESIAN_POINT ( 'NONE',  ( 2.500000000000000000, 0.000000000000000000, 0.000000000000000000 ) ) ;
#32687=EDGE_CURVE ( 'NONE', #27345, #1527, #30326, .T. ) ;
#32709=CARTESIAN_POINT ( 'NONE',  ( 21.00000000000000355, 0.000000000000000000, 2.055000000000000160 ) ) ;
#32989=PRESENTATION_STYLE_ASSIGNMENT (( #57062 ) ) ;
#32990=LINE ( 'NONE', #14192, #56188 ) ;
#33118=DIRECTION ( 'NONE',  ( -1.000000000000000000, -0.000000000000000000, -0.000000000000000000 ) ) ;
#33253=DIRECTION ( 'NONE',  ( 0.000000000000000000, 0.000000000000000000, 1.000000000000000000 ) ) ;
#33535=CARTESIAN_POINT ( 'NONE',  ( 5.200000000000002842, 0.000000000000000000, 0.000000000000000000 ) ) ;
#33681=EDGE_CURVE ( 'NONE', #40146, #16747, #55419, .T. ) ;
#33774=CONICAL_SURFACE ( 'NONE', #6705, 2.055000000000000160, 0.7853981633974639331 ) ;
#33936=DIRECTION ( 'NONE',  ( 0.000000000000000000, 0.000000000000000000, 1.000000000000000000 ) ) ;
#34225=CARTESIAN_POINT ( 'NONE',  ( 0.2500000000000002220, 4.898587196589412829E-16, -4.000000000000000000 ) ) ;
#34453=ADVANCED_FACE ( 'NONE', ( #21103 ), #3410, .T. ) ;
#34466=DIRECTION ( 'NONE',  ( 0.000000000000000000, 0.000000000000000000, -1.000000000000000000 ) ) ;
#34532=AXIS2_PLACEMENT_3D ( 'NONE', #17450, #22763, #40981 ) ;
#34542=EDGE_CURVE ( 'NONE', #2015, #5057, #32990, .T. ) ;
#34551=ORIENTED_EDGE ( 'NONE', *, *, #39281, .T. ) ;
#34573=CARTESIAN_POINT ( 'NONE',  ( 5.000000000000000888, 4.250000000000000000, 0.000000000000000000 ) ) ;
#34860=STYLED_ITEM ( 'NONE', ( #32204 ), #35493 ) ;
#34920=PLANE ( 'NONE',  #61500 ) ;
#34947=DIRECTION ( 'NONE',  ( 0.000000000000000000, 0.000000000000000000, 1.000000000000000000 ) ) ;
#34998=VECTOR ( 'NONE', #60860, 1000.000000000000114 ) ;
#35220=VERTEX_POINT ( 'NONE', #43199 ) ;
#35225=ORIENTED_EDGE ( 'NONE', *, *, #53172, .T. ) ;
#35297=FACE_BOUND ( 'NONE', #13853, .T. ) ;
#35434=DIRECTION ( 'NONE',  ( 0.000000000000000000, 0.5000000000000009992, 0.8660254037844380415 ) ) ;
#35493=ADVANCED_BREP_SHAPE_REPRESENTATION ( '', ( #30720, #14677 ), #38903 ) ;
#35571=DIRECTION ( 'NONE',  ( 0.000000000000000000, 1.000000000000000000, -1.287488025362403787E-15 ) ) ;
#35610=CIRCLE ( 'NONE', #8557, 0.2000000000000000944 ) ;
#35615=DIRECTION ( 'NONE',  ( -0.000000000000000000, 0.000000000000000000, 1.000000000000000000 ) ) ;
#35645=ORIENTED_EDGE ( 'NONE', *, *, #12189, .F. ) ;
#35646=DIRECTION ( 'NONE',  ( 0.000000000000000000, 0.000000000000000000, 1.000000000000000000 ) ) ;
#35664=VERTEX_POINT ( 'NONE', #37189 ) ;
#35733=DIRECTION ( 'NONE',  ( 0.000000000000000000, 0.000000000000000000, -1.000000000000000000 ) ) ;
#35775=VERTEX_POINT ( 'NONE', #58102 ) ;
#35815=CIRCLE ( 'NONE', #6731, 2.700000000000000622 ) ;
#35948=CARTESIAN_POINT ( 'NONE',  ( 2.500000000000000000, 2.357898499370431722, -2.818925648462311528E-15 ) ) ;
#35976=CARTESIAN_POINT ( 'NONE',  ( 2.500000000000000000, -1.178949249685214307, 2.042000000000001592 ) ) ;
#36146=DIRECTION ( 'NONE',  ( -1.000000000000000000, -0.000000000000000000, -0.000000000000000000 ) ) ;
#36260=FACE_OUTER_BOUND ( 'NONE', #52272, .T. ) ;
#36297=( NAMED_UNIT ( * ) SI_UNIT ( $, .STERADIAN. ) SOLID_ANGLE_UNIT ( ) );
#36452=FACE_OUTER_BOUND ( 'NONE', #50406, .T. ) ;
#36459=ORIENTED_EDGE ( 'NONE', *, *, #52982, .T. ) ;
#36461=EDGE_CURVE ( 'NONE', #23179, #22826, #16225, .T. ) ;
#36463=FACE_OUTER_BOUND ( 'NONE', #42263, .T. ) ;
#36493=DIRECTION ( 'NONE',  ( 0.000000000000000000, -1.287488025362403787E-15, -1.000000000000000000 ) ) ;
#36498=PLANE ( 'NONE',  #19508 ) ;
#36548=CARTESIAN_POINT ( 'NONE',  ( 21.00000000000000355, 0.000000000000000000, 2.055000000000000160 ) ) ;
#36567=CYLINDRICAL_SURFACE ( 'NONE', #14763, 2.500000000000000444 ) ;
#36581=DIRECTION ( 'NONE',  ( -1.000000000000000000, -0.000000000000000000, -0.000000000000000000 ) ) ;
#36697=DIRECTION ( 'NONE',  ( 1.000000000000000000, 0.000000000000000000, 0.000000000000000000 ) ) ;
#36813=CARTESIAN_POINT ( 'NONE',  ( 2.500000000000000000, 2.357898499370431722, -2.818925648462311528E-15 ) ) ;
#36859=EDGE_LOOP ( 'NONE', ( #50550, #28815, #43164, #50650 ) ) ;
#36905=FACE_OUTER_BOUND ( 'NONE', #61083, .T. ) ;
#36935=DIRECTION ( 'NONE',  ( -1.000000000000000000, -0.000000000000000000, -0.000000000000000000 ) ) ;
#37189=CARTESIAN_POINT ( 'NONE',  ( 2.500000000000000000, -1.768423874527825568, -1.020999999999998575 ) ) ;
#37390=CIRCLE ( 'NONE', #12390, 4.000000000000000000 ) ;
#37391=UNCERTAINTY_MEASURE_WITH_UNIT (LENGTH_MEASURE( 1.000000000000000082E-05 ), #22795, 'distance_accuracy_value', 'NONE');
#37460=DIRECTION ( 'NONE',  ( 0.000000000000000000, -0.5000000000000009992, -0.8660254037844380415 ) ) ;
#37617=EDGE_CURVE ( 'NONE', #35664, #43133, #53721, .T. ) ;
#37728=AXIS2_PLACEMENT_3D ( 'NONE', #33535, #282, #20354 ) ;
#37873=DIRECTION ( 'NONE',  ( -1.000000000000000000, -0.000000000000000000, -0.000000000000000000 ) ) ;
#37970=ORIENTED_EDGE ( 'NONE', *, *, #4294, .F. ) ;
#38280=ORIENTED_EDGE ( 'NONE', *, *, #3895, .T. ) ;
#38368=DIRECTION ( 'NONE',  ( 0.000000000000000000, -0.4999999999999993339, 0.8660254037844390407 ) ) ;
#38435=CARTESIAN_POINT ( 'NONE',  ( 2.500000000000000000, 2.357898499370431722, -2.818925648462311528E-15 ) ) ;
#38437=CONICAL_SURFACE ( 'NONE', #41480, 2.055000000000000160, 0.7853981633974639331 ) ;
#38600=CARTESIAN_POINT ( 'NONE',  ( 2.500000000000000000, 1.178949249685217415, 2.041999999999998483 ) ) ;
#38613=( NAMED_UNIT ( * ) SI_UNIT ( $, .STERADIAN. ) SOLID_ANGLE_UNIT ( ) );
#38650=CARTESIAN_POINT ( 'NONE',  ( 0.000000000000000000, 2.357898499370431722, -2.818925648462311528E-15 ) ) ;
#38736=DIRECTION ( 'NONE',  ( 0.000000000000000000, 0.000000000000000000, -1.000000000000000000 ) ) ;
#38876=AXIS2_PLACEMENT_3D ( 'NONE', #54435, #1825, #20953 ) ;
#38903=( GEOMETRIC_REPRESENTATION_CONTEXT ( 3 ) GLOBAL_UNCERTAINTY_ASSIGNED_CONTEXT ( ( #37391 ) ) GLOBAL_UNIT_ASSIGNED_CONTEXT ( ( #22795, #51587, #23111 ) ) REPRESENTATION_CONTEXT ( 'NONE', 'WORKASPACE' ) );
#38962=CIRCLE ( 'NONE', #45988, 2.041999999999999815 ) ;
#39004=AXIS2_PLACEMENT_3D ( 'NONE', #34225, #24189, #29195 ) ;
#39108=ORIENTED_EDGE ( 'NONE', *, *, #32687, .T. ) ;
#39232=LINE ( 'NONE', #14487, #22129 ) ;
#39236=VECTOR ( 'NONE', #60942, 1000.000000000000114 ) ;
#39281=EDGE_CURVE ( 'NONE', #44200, #45745, #54748, .T. ) ;
#39407=DIRECTION ( 'NONE',  ( 0.000000000000000000, 0.000000000000000000, 1.000000000000000000 ) ) ;
#39592=ORIENTED_EDGE ( 'NONE', *, *, #770, .F. ) ;
#39722=DIRECTION ( 'NONE',  ( -1.000000000000000000, -0.000000000000000000, -0.000000000000000000 ) ) ;
#39727=CARTESIAN_POINT ( 'NONE',  ( 0.000000000000000000, 0.000000000000000000, 4.000000000000000000 ) ) ;
#39747=CARTESIAN_POINT ( 'NONE',  ( 5.000000000000000888, 0.000000000000000000, 0.000000000000000000 ) ) ;
#39783=AXIS2_PLACEMENT_3D ( 'NONE', #18449, #5244, #28447 ) ;
#39793=EDGE_LOOP ( 'NONE', ( #42183, #3577, #60064 ) ) ;
#39833=CARTESIAN_POINT ( 'NONE',  ( 21.00000000000000355, 0.000000000000000000, 0.000000000000000000 ) ) ;
#39906=CIRCLE ( 'NONE', #5859, 4.250000000000000000 ) ;
#40121=DIRECTION ( 'NONE',  ( 0.000000000000000000, 0.000000000000000000, -1.000000000000000000 ) ) ;
#40146=VERTEX_POINT ( 'NONE', #43441 ) ;
#40168=DIRECTION ( 'NONE',  ( 0.000000000000000000, 0.000000000000000000, 1.000000000000000000 ) ) ;
#40328=CARTESIAN_POINT ( 'NONE',  ( 2.500000000000000000, 2.357898499370431722, -2.818925648462311528E-15 ) ) ;
#40650=CARTESIAN_POINT ( 'NONE',  ( -31.74999999999995737, 0.000000000000000000, 2.500000000000000444 ) ) ;
#40865=VECTOR ( 'NONE', #11453, 1000.000000000000000 ) ;
#40901=ADVANCED_FACE ( 'NONE', ( #6248 ), #25703, .T. ) ;
#40925=ORIENTED_EDGE ( 'NONE', *, *, #2597, .T. ) ;
#40981=DIRECTION ( 'NONE',  ( 0.000000000000000000, 0.000000000000000000, -1.000000000000000000 ) ) ;
#40982=ADVANCED_FACE ( 'NONE', ( #43812 ), #21680, .T. ) ;
#41287=ORIENTED_EDGE ( 'NONE', *, *, #46232, .T. ) ;
#41292=PLANE ( 'NONE',  #59491 ) ;
#41326=EDGE_CURVE ( 'NONE', #15399, #49037, #7665, .T. ) ;
#41480=AXIS2_PLACEMENT_3D ( 'NONE', #53338, #1028, #19550 ) ;
#41520=VECTOR ( 'NONE', #38368, 1000.000000000000000 ) ;
#41593=DIRECTION ( 'NONE',  ( 0.000000000000000000, -0.5000000000000009992, -0.8660254037844380415 ) ) ;
#41711=CARTESIAN_POINT ( 'NONE',  ( 2.500000000000000000, 1.178949249685217415, 2.041999999999998483 ) ) ;
#41727=ORIENTED_EDGE ( 'NONE', *, *, #24008, .F. ) ;
#41866=CARTESIAN_POINT ( 'NONE',  ( 2.500000000000000000, -1.768423874527823569, 1.021000000000002350 ) ) ;
#41927=( NAMED_UNIT ( * ) PLANE_ANGLE_UNIT ( ) SI_UNIT ( $, .RADIAN. ) );
#42028=EDGE_CURVE ( 'NONE', #45745, #44200, #28744, .T. ) ;
#42091=( LENGTH_UNIT ( ) NAMED_UNIT ( * ) SI_UNIT ( .MILLI., .METRE. ) );
#42171=LINE ( 'NONE', #122, #11320 ) ;
#42183=ORIENTED_EDGE ( 'NONE', *, *, #27732, .T. ) ;
#42202=ADVANCED_FACE ( 'NONE', ( #36260 ), #36567, .T. ) ;
#42226=ORIENTED_EDGE ( 'NONE', *, *, #20397, .T. ) ;
#42263=EDGE_LOOP ( 'NONE', ( #39592, #13008, #16683, #42322, #2811 ) ) ;
#42283=CARTESIAN_POINT ( 'NONE',  ( 0.000000000000000000, 0.000000000000000000, 0.000000000000000000 ) ) ;
#42292=CARTESIAN_POINT ( 'NONE',  ( 20.55500000000001748, 0.000000000000000000, 0.000000000000000000 ) ) ;
#42312=DIRECTION ( 'NONE',  ( 0.000000000000000000, -0.5000000000000009992, -0.8660254037844380415 ) ) ;
#42322=ORIENTED_EDGE ( 'NONE', *, *, #48978, .T. ) ;
#42323=CARTESIAN_POINT ( 'NONE',  ( 0.000000000000000000, -1.178949249685218748, -2.041999999999998039 ) ) ;
#42402=DIRECTION ( 'NONE',  ( 0.000000000000000000, -1.000000000000000000, 1.287488025362403787E-15 ) ) ;
#42458=ADVANCED_FACE ( 'NONE', ( #1700 ), #50737, .F. ) ;
#42528=EDGE_CURVE ( 'NONE', #1527, #3705, #44976, .T. ) ;
#42531=ADVANCED_FACE ( 'NONE', ( #11759 ), #27076, .F. ) ;
#42710=AXIS2_PLACEMENT_3D ( 'NONE', #14218, #18918, #33936 ) ;
#43133=VERTEX_POINT ( 'NONE', #14624 ) ;
#43164=ORIENTED_EDGE ( 'NONE', *, *, #29056, .T. ) ;
#43199=CARTESIAN_POINT ( 'NONE',  ( 5.000000000000002665, 0.000000000000000000, -2.700000000000000622 ) ) ;
#43303=CIRCLE ( 'NONE', #46293, 4.000000000000000000 ) ;
#43351=LINE ( 'NONE', #38650, #58228 ) ;
#43441=CARTESIAN_POINT ( 'NONE',  ( 21.00000000000000355, 2.789133085058097101E-16, -2.055000000000000160 ) ) ;
#43647=ADVANCED_FACE ( 'NONE', ( #24545, #53039 ), #5710, .T. ) ;
#43702=CYLINDRICAL_SURFACE ( 'NONE', #11691, 2.500000000000000444 ) ;
#43738=ORIENTED_EDGE ( 'NONE', *, *, #33681, .F. ) ;
#43790=CARTESIAN_POINT ( 'NONE',  ( 2.500000000000000000, 0.000000000000000000, 0.000000000000000000 ) ) ;
#43812=FACE_OUTER_BOUND ( 'NONE', #10346, .T. ) ;
#43824=CARTESIAN_POINT ( 'NONE',  ( 2.500000000000000000, 1.178949249685212974, -2.042000000000001148 ) ) ;
#44030=VECTOR ( 'NONE', #39722, 1000.000000000000000 ) ;
#44099=EDGE_CURVE ( 'NONE', #50629, #35664, #38962, .T. ) ;
#44126=VECTOR ( 'NONE', #11347, 1000.000000000000000 ) ;
#44128=EDGE_LOOP ( 'NONE', ( #20328, #12613, #13771 ) ) ;
#44196=PLANE ( 'NONE',  #54033 ) ;
#44200=VERTEX_POINT ( 'NONE', #27869 ) ;
#44260=DIRECTION ( 'NONE',  ( 0.000000000000000000, 0.000000000000000000, 1.000000000000000000 ) ) ;
#44381=VECTOR ( 'NONE', #2738, 1000.000000000000000 ) ;
#44417=ORIENTED_EDGE ( 'NONE', *, *, #973, .T. ) ;
#44446=ORIENTED_EDGE ( 'NONE', *, *, #45373, .T. ) ;
#44716=CARTESIAN_POINT ( 'NONE',  ( 2.500000000000000000, 2.357898499370431722, -2.818925648462311528E-15 ) ) ;
#44844=DIRECTION ( 'NONE',  ( 0.000000000000000000, 0.8660254037844380415, -0.5000000000000009992 ) ) ;
#44976=LINE ( 'NONE', #55250, #20878 ) ;
#45045=AXIS2_PLACEMENT_3D ( 'NONE', #32627, #8806, #33253 ) ;
#45237=DIRECTION ( 'NONE',  ( 0.000000000000000000, -0.5000000000000013323, -0.8660254037844380415 ) ) ;
#45296=LINE ( 'NONE', #30539, #40865 ) ;
#45309=DIRECTION ( 'NONE',  ( 0.000000000000000000, 0.000000000000000000, 1.000000000000000000 ) ) ;
#45355=DIRECTION ( 'NONE',  ( -1.000000000000000000, -0.000000000000000000, -0.000000000000000000 ) ) ;
#45373=EDGE_CURVE ( 'NONE', #30367, #35775, #7387, .T. ) ;
#45375=DIRECTION ( 'NONE',  ( 0.000000000000000000, 0.000000000000000000, -1.000000000000000000 ) ) ;
#45499=AXIS2_PLACEMENT_3D ( 'NONE', #13392, #33118, #61885 ) ;
#45695=SURFACE_STYLE_USAGE ( .BOTH. , #31269 ) ;
#45741=PLANE ( 'NONE',  #5384 ) ;
#45745=VERTEX_POINT ( 'NONE', #3235 ) ;
#45795=ORIENTED_EDGE ( 'NONE', *, *, #2679, .T. ) ;
#45981=CIRCLE ( 'NONE', #3937, 2.500000000000000888 ) ;
#45988=AXIS2_PLACEMENT_3D ( 'NONE', #31645, #1571, #20706 ) ;
#46094=EDGE_CURVE ( 'NONE', #19831, #50629, #21015, .T. ) ;
#46166=CARTESIAN_POINT ( 'NONE',  ( 0.2500000000000002220, 0.000000000000000000, 0.000000000000000000 ) ) ;
#46212=EDGE_CURVE ( 'NONE', #23179, #19831, #54706, .T. ) ;
#46232=EDGE_CURVE ( 'NONE', #22826, #19831, #29012, .T. ) ;
#46244=CARTESIAN_POINT ( 'NONE',  ( 0.000000000000000000, 1.178949249685212974, -2.042000000000001148 ) ) ;
#46267=PLANE ( 'NONE',  #6802 ) ;
#46293=AXIS2_PLACEMENT_3D ( 'NONE', #42283, #4948, #24077 ) ;
#46454=LINE ( 'NONE', #38600, #56836 ) ;
#46473=DIRECTION ( 'NONE',  ( -1.000000000000000000, -0.000000000000000000, -0.000000000000000000 ) ) ;
#46489=ORIENTED_EDGE ( 'NONE', *, *, #17549, .F. ) ;
#46611=DIRECTION ( 'NONE',  ( 0.000000000000000000, 0.000000000000000000, -1.000000000000000000 ) ) ;
#46664=CIRCLE ( 'NONE', #17631, 0.2000000000000000944 ) ;
#46772=CYLINDRICAL_SURFACE ( 'NONE', #31852, 4.250000000000000000 ) ;
#47060=LINE ( 'NONE', #28533, #47535 ) ;
#47063=ORIENTED_EDGE ( 'NONE', *, *, #4714, .T. ) ;
#47101=LINE ( 'NONE', #9478, #34998 ) ;
#47144=VECTOR ( 'NONE', #61438, 1000.000000000000000 ) ;
#47204=ADVANCED_FACE ( 'NONE', ( #20694 ), #33774, .T. ) ;
#47342=ORIENTED_EDGE ( 'NONE', *, *, #44099, .F. ) ;
#47535=VECTOR ( 'NONE', #4097, 1000.000000000000114 ) ;
#47552=EDGE_CURVE ( 'NONE', #30367, #2015, #51804, .T. ) ;
#47723=DIRECTION ( 'NONE',  ( 0.000000000000000000, 0.000000000000000000, -1.000000000000000000 ) ) ;
#48260=ORIENTED_EDGE ( 'NONE', *, *, #46232, .F. ) ;
#48267=ORIENTED_EDGE ( 'NONE', *, *, #36461, .F. ) ;
#48310=ORIENTED_EDGE ( 'NONE', *, *, #13073, .T. ) ;
#48312=VERTEX_POINT ( 'NONE', #1265 ) ;
#48782=APPLICATION_CONTEXT ( 'automotive_design' ) ;
#48978=EDGE_CURVE ( 'NONE', #35664, #15368, #55828, .T. ) ;
#49037=VERTEX_POINT ( 'NONE', #9225 ) ;
#49048=VECTOR ( 'NONE', #6997, 1000.000000000000114 ) ;
#49167=DIRECTION ( 'NONE',  ( 1.000000000000000000, 0.000000000000000000, 0.000000000000000000 ) ) ;
#49229=DIRECTION ( 'NONE',  ( -1.000000000000000000, -0.000000000000000000, -0.000000000000000000 ) ) ;
#49290=EDGE_CURVE ( 'NONE', #1527, #21489, #24105, .T. ) ;
#49355=ADVANCED_FACE ( 'NONE', ( #271 ), #30641, .T. ) ;
#49365=VECTOR ( 'NONE', #20602, 1000.000000000000000 ) ;
#49376=DIRECTION ( 'NONE',  ( -1.000000000000000000, 0.000000000000000000, -0.000000000000000000 ) ) ;
#49381=LINE ( 'NONE', #40328, #55061 ) ;
#49585=LINE ( 'NONE', #20182, #59868 ) ;
#49787=FACE_OUTER_BOUND ( 'NONE', #52367, .T. ) ;
#50033=CARTESIAN_POINT ( 'NONE',  ( -31.74999999999995737, 0.000000000000000000, 0.000000000000000000 ) ) ;
#50047=DIRECTION ( 'NONE',  ( 0.000000000000000000, -0.4999999999999993339, 0.8660254037844390407 ) ) ;
#50068=EDGE_CURVE ( 'NONE', #40146, #2015, #42171, .T. ) ;
#50124=ORIENTED_EDGE ( 'NONE', *, *, #2597, .F. ) ;
#50193=ORIENTED_EDGE ( 'NONE', *, *, #9907, .T. ) ;
#50218=CYLINDRICAL_SURFACE ( 'NONE', #54669, 4.250000000000000000 ) ;
#50406=EDGE_LOOP ( 'NONE', ( #57193, #34551, #36459, #60402 ) ) ;
#50550=ORIENTED_EDGE ( 'NONE', *, *, #4798, .F. ) ;
#50629=VERTEX_POINT ( 'NONE', #27221 ) ;
#50650=ORIENTED_EDGE ( 'NONE', *, *, #32057, .F. ) ;
#50651=LINE ( 'NONE', #35976, #6485 ) ;
#50733=ORIENTED_EDGE ( 'NONE', *, *, #17549, .T. ) ;
#50737=TOROIDAL_SURFACE ( 'NONE', #23741, 2.700000000000000622, 0.2000000000000000111 ) ;
#50850=EDGE_CURVE ( 'NONE', #376, #50629, #6154, .T. ) ;
#50883=CIRCLE ( 'NONE', #11932, 0.2500000000000002220 ) ;
#50919=ORIENTED_EDGE ( 'NONE', *, *, #27732, .F. ) ;
#51153=APPLICATION_CONTEXT ( 'automotive_design' ) ;
#51154=ORIENTED_EDGE ( 'NONE', *, *, #10301, .T. ) ;
#51210=LINE ( 'NONE', #18035, #22469 ) ;
#51284=( LENGTH_UNIT ( ) NAMED_UNIT ( * ) SI_UNIT ( .MILLI., .METRE. ) );
#51330=FACE_OUTER_BOUND ( 'NONE', #59020, .T. ) ;
#51587=( NAMED_UNIT ( * ) PLANE_ANGLE_UNIT ( ) SI_UNIT ( $, .RADIAN. ) );
#51751=ADVANCED_FACE ( 'NONE', ( #51330 ), #45741, .T. ) ;
#51753=( NAMED_UNIT ( * ) PLANE_ANGLE_UNIT ( ) SI_UNIT ( $, .RADIAN. ) );
#51804=CIRCLE ( 'NONE', #5769, 2.500000000000000888 ) ;
#51848=AXIS2_PLACEMENT_3D ( 'NONE', #30869, #21170, #45309 ) ;
#52217=ORIENTED_EDGE ( 'NONE', *, *, #46212, .T. ) ;
#52237=ORIENTED_EDGE ( 'NONE', *, *, #31604, .F. ) ;
#52272=EDGE_LOOP ( 'NONE', ( #6597, #28207, #48310, #15417 ) ) ;
#52335=EDGE_LOOP ( 'NONE', ( #16834, #12506, #50919, #11067, #24918 ) ) ;
#52367=EDGE_LOOP ( 'NONE', ( #7724, #9089, #6226, #46489 ) ) ;
#52372=ADVANCED_FACE ( 'NONE', ( #19859 ), #38437, .T. ) ;
#52402=DIRECTION ( 'NONE',  ( 0.000000000000000000, -1.000000000000000000, 0.000000000000000000 ) ) ;
#52840=TOROIDAL_SURFACE ( 'NONE', #11870, 2.700000000000000622, 0.2000000000000000111 ) ;
#52900=EDGE_CURVE ( 'NONE', #15368, #18903, #17495, .T. ) ;
#52935=VECTOR ( 'NONE', #888, 1000.000000000000000 ) ;
#52982=EDGE_CURVE ( 'NONE', #45745, #15399, #5489, .T. ) ;
#53001=VECTOR ( 'NONE', #26214, 999.9999999999997726 ) ;
#53039=FACE_OUTER_BOUND ( 'NONE', #21855, .T. ) ;
#53172=EDGE_CURVE ( 'NONE', #48312, #3705, #3882, .T. ) ;
#53279=DIRECTION ( 'NONE',  ( -1.000000000000000000, -0.000000000000000000, -0.000000000000000000 ) ) ;
#53338=CARTESIAN_POINT ( 'NONE',  ( 21.00000000000000355, 0.000000000000000000, 0.000000000000000000 ) ) ;
#53372=DIRECTION ( 'NONE',  ( 0.000000000000000000, -1.000000000000000000, 1.287488025362403787E-15 ) ) ;
#53535=FACE_OUTER_BOUND ( 'NONE', #54481, .T. ) ;
#53635=DIRECTION ( 'NONE',  ( 0.000000000000000000, 0.000000000000000000, -1.000000000000000000 ) ) ;
#53684=CONICAL_SURFACE ( 'NONE', #25677, 2.041999999999999815, 1.047197551196591858 ) ;
#53721=LINE ( 'NONE', #10855, #649 ) ;
#53803=ORIENTED_EDGE ( 'NONE', *, *, #52982, .F. ) ;
#53917=CARTESIAN_POINT ( 'NONE',  ( 2.500000000000000000, -1.178949249685218748, -2.041999999999998039 ) ) ;
#54030=CARTESIAN_POINT ( 'NONE',  ( -31.74999999999995737, 0.000000000000000000, 4.250000000000000000 ) ) ;
#54033=AXIS2_PLACEMENT_3D ( 'NONE', #5598, #15359, #34466 ) ;
#54099=CARTESIAN_POINT ( 'NONE',  ( 2.500000000000000000, 2.357898499370431722, -2.818925648462311528E-15 ) ) ;
#54226=EDGE_LOOP ( 'NONE', ( #47063, #8574, #3616, #58257, #633 ) ) ;
#54227=CARTESIAN_POINT ( 'NONE',  ( -31.74999999999995737, 5.204748896376250699E-16, -4.250000000000000000 ) ) ;
#54242=STYLED_ITEM ( 'NONE', ( #32989 ), #30720 ) ;
#54368=ORIENTED_EDGE ( 'NONE', *, *, #31598, .F. ) ;
#54395=CARTESIAN_POINT ( 'NONE',  ( 2.500000000000000000, 2.357898499370431722, -2.818925648462311528E-15 ) ) ;
#54435=CARTESIAN_POINT ( 'NONE',  ( 2.500000000000000000, -2.357898499370432166, 3.035766082959412415E-15 ) ) ;
#54481=EDGE_LOOP ( 'NONE', ( #1047, #56007, #47342 ) ) ;
#54669=AXIS2_PLACEMENT_3D ( 'NONE', #11713, #36146, #2593 ) ;
#54676=CARTESIAN_POINT ( 'NONE',  ( 5.000000000000000888, 0.000000000000000000, 0.000000000000000000 ) ) ;
#54706=LINE ( 'NONE', #54395, #53001 ) ;
#54721=ADVANCED_FACE ( 'NONE', ( #55637 ), #8648, .F. ) ;
#54727=ORIENTED_EDGE ( 'NONE', *, *, #23280, .T. ) ;
#54748=CIRCLE ( 'NONE', #27755, 4.250000000000000000 ) ;
#54777=ORIENTED_EDGE ( 'NONE', *, *, #17457, .T. ) ;
#54780=ORIENTED_EDGE ( 'NONE', *, *, #13980, .T. ) ;
#54967=CARTESIAN_POINT ( 'NONE',  ( 2.500000000000000000, -1.178949249685214307, 2.042000000000001592 ) ) ;
#55015=ADVANCED_FACE ( 'NONE', ( #31469 ), #36498, .F. ) ;
#55040=DIRECTION ( 'NONE',  ( 0.000000000000000000, 0.000000000000000000, 1.000000000000000000 ) ) ;
#55055=CARTESIAN_POINT ( 'NONE',  ( 21.00000000000000000, 2.055000000000000160, 0.000000000000000000 ) ) ;
#55057=FILL_AREA_STYLE_COLOUR ( '', #11893 ) ;
#55061=VECTOR ( 'NONE', #26499, 1000.000000000000000 ) ;
#55233=ORIENTED_EDGE ( 'NONE', *, *, #770, .T. ) ;
#55250=CARTESIAN_POINT ( 'NONE',  ( 0.000000000000000000, -1.178949249685214307, 2.042000000000001592 ) ) ;
#55419=CIRCLE ( 'NONE', #5369, 2.055000000000000160 ) ;
#55525=DIRECTION ( 'NONE',  ( -1.000000000000000000, -0.000000000000000000, -0.000000000000000000 ) ) ;
#55529=CARTESIAN_POINT ( 'NONE',  ( 2.500000000000000000, 0.000000000000000000, 0.000000000000000000 ) ) ;
#55637=FACE_OUTER_BOUND ( 'NONE', #58568, .T. ) ;
#55828=CIRCLE ( 'NONE', #51848, 2.041999999999999815 ) ;
#55979=DIRECTION ( 'NONE',  ( 0.000000000000000000, -1.000000000000000000, 0.000000000000000000 ) ) ;
#56007=ORIENTED_EDGE ( 'NONE', *, *, #37617, .F. ) ;
#56133=FACE_OUTER_BOUND ( 'NONE', #22385, .T. ) ;
#56162=PRODUCT_DEFINITION_CONTEXT ( 'detailed design', #48782, 'design' ) ;
#56188=VECTOR ( 'NONE', #18892, 1000.000000000000000 ) ;
#56275=AXIS2_PLACEMENT_3D ( 'NONE', #39747, #30307, #58798 ) ;
#56307=ORIENTED_EDGE ( 'NONE', *, *, #4841, .F. ) ;
#56608=CARTESIAN_POINT ( 'NONE',  ( 5.200000000000002842, 3.306546357697854226E-16, 2.700000000000000622 ) ) ;
#56630=ORIENTED_EDGE ( 'NONE', *, *, #32057, .T. ) ;
#56836=VECTOR ( 'NONE', #53279, 1000.000000000000000 ) ;
#57013=ORIENTED_EDGE ( 'NONE', *, *, #16857, .F. ) ;
#57062=SURFACE_STYLE_USAGE ( .BOTH. , #19198 ) ;
#57193=ORIENTED_EDGE ( 'NONE', *, *, #973, .F. ) ;
#57815=DIRECTION ( 'NONE',  ( 0.000000000000000000, 0.4999999999999990008, -0.8660254037844391517 ) ) ;
#57869=ADVANCED_FACE ( 'NONE', ( #19901 ), #34920, .F. ) ;
#57870=VERTEX_POINT ( 'NONE', #29886 ) ;
#57913=AXIS2_PLACEMENT_3D ( 'NONE', #34573, #723, #53635 ) ;
#58070=CARTESIAN_POINT ( 'NONE',  ( 2.500000000000000000, -1.178949249685214307, 2.042000000000001592 ) ) ;
#58102=CARTESIAN_POINT ( 'NONE',  ( 5.200000000000002842, 0.000000000000000000, 2.500000000000000444 ) ) ;
#58161=ORIENTED_EDGE ( 'NONE', *, *, #22781, .T. ) ;
#58195=EDGE_LOOP ( 'NONE', ( #27139, #3839, #45795, #19591, #13360 ) ) ;
#58228=VECTOR ( 'NONE', #18607, 999.9999999999997726 ) ;
#58257=ORIENTED_EDGE ( 'NONE', *, *, #50850, .F. ) ;
#58358=FACE_OUTER_BOUND ( 'NONE', #12607, .T. ) ;
#58438=FACE_OUTER_BOUND ( 'NONE', #19709, .T. ) ;
#58524=ORIENTED_EDGE ( 'NONE', *, *, #34542, .F. ) ;
#58566=EDGE_LOOP ( 'NONE', ( #26370, #6767, #19075 ) ) ;
#58568=EDGE_LOOP ( 'NONE', ( #48267, #52217, #48260 ) ) ;
#58678=AXIS2_PLACEMENT_3D ( 'NONE', #25390, #44844, #35434 ) ;
#58798=DIRECTION ( 'NONE',  ( 0.000000000000000000, 0.000000000000000000, -1.000000000000000000 ) ) ;
#58888=PRODUCT_DEFINITION_FORMATION_WITH_SPECIFIED_SOURCE ( 'ANY', '', #8800, .NOT_KNOWN. ) ;
#59020=EDGE_LOOP ( 'NONE', ( #16604, #54368, #28355, #19592, #51154 ) ) ;
#59230=CARTESIAN_POINT ( 'NONE',  ( 20.55500000000001748, 0.000000000000000000, 0.000000000000000000 ) ) ;
#59491=AXIS2_PLACEMENT_3D ( 'NONE', #16862, #26232, #45375 ) ;
#59638=ORIENTED_EDGE ( 'NONE', *, *, #42528, .F. ) ;
#59701=DIRECTION ( 'NONE',  ( 1.000000000000000000, 0.000000000000000000, 0.000000000000000000 ) ) ;
#59868=VECTOR ( 'NONE', #45237, 999.9999999999997726 ) ;
#59899=CONICAL_SURFACE ( 'NONE', #878, 2.041999999999999815, 1.047197551196591858 ) ;
#59938=UNCERTAINTY_MEASURE_WITH_UNIT (LENGTH_MEASURE( 1.000000000000000082E-05 ), #42091, 'distance_accuracy_value', 'NONE');
#60002=FACE_OUTER_BOUND ( 'NONE', #15552, .T. ) ;
#60050=AXIS2_PLACEMENT_3D ( 'NONE', #1746, #49376, #35615 ) ;
#60064=ORIENTED_EDGE ( 'NONE', *, *, #46094, .F. ) ;
#60080=VECTOR ( 'NONE', #42402, 1000.000000000000000 ) ;
#60194=ORIENTED_EDGE ( 'NONE', *, *, #42028, .T. ) ;
#60212=CARTESIAN_POINT ( 'NONE',  ( -31.74999999999995737, 0.000000000000000000, 0.000000000000000000 ) ) ;
#60242=LINE ( 'NONE', #7948, #49048 ) ;
#60260=DIRECTION ( 'NONE',  ( 0.000000000000000000, 1.000000000000000000, -1.287488025362403787E-15 ) ) ;
#60348=CARTESIAN_POINT ( 'NONE',  ( 2.500000000000000000, 0.000000000000000000, 0.000000000000000000 ) ) ;
#60402=ORIENTED_EDGE ( 'NONE', *, *, #41326, .T. ) ;
#60860=DIRECTION ( 'NONE',  ( 0.000000000000000000, 0.4999999999999990008, -0.8660254037844391517 ) ) ;
#60942=DIRECTION ( 'NONE',  ( -0.7071067811865364705, 0.000000000000000000, 0.7071067811865584529 ) ) ;
#61079=DIRECTION ( 'NONE',  ( 0.000000000000000000, 0.000000000000000000, 1.000000000000000000 ) ) ;
#61083=EDGE_LOOP ( 'NONE', ( #40925, #37970, #26915 ) ) ;
#61322=ORIENTED_EDGE ( 'NONE', *, *, #31604, .T. ) ;
#61387=DIRECTION ( 'NONE',  ( 0.000000000000000000, 0.000000000000000000, 1.000000000000000000 ) ) ;
#61438=DIRECTION ( 'NONE',  ( 0.000000000000000000, 1.000000000000000000, -1.287488025362403787E-15 ) ) ;
#61500=AXIS2_PLACEMENT_3D ( 'NONE', #58070, #15191, #53372 ) ;
#61576=ADVANCED_FACE ( 'NONE', ( #2171 ), #11934, .F. ) ;
#61885=DIRECTION ( 'NONE',  ( 0.000000000000000000, 0.000000000000000000, 1.000000000000000000 ) ) ;
ENDSEC;
END-ISO-10303-21;
